ISO-10303-21;
HEADER;
/* Generated by software containing ST-Developer
 * from STEP Tools, Inc. (www.steptools.com) 
 */

FILE_DESCRIPTION(
/* description */ ('Cam-driven reciprocating slide'),
/* implementation_level */ '2;1');

FILE_NAME(
/* name */ 'M4x10 Cap Screw.step',
/* time_stamp */ '2026-10-28T03:25:20-07:00',
/* author */ (''),
/* organization */ (''),
/* preprocessor_version */ 'ST-DEVELOPER v20.2',
/* originating_system */ 'Autodesk Translation Framework v15.17.0.0',
/* authorisation */ '');

FILE_SCHEMA (('AUTOMOTIVE_DESIGN { 1 0 10303 214 3 1 1 }'));
ENDSEC;

DATA;
#10=MECHANICAL_DESIGN_GEOMETRIC_PRESENTATION_REPRESENTATION('',(#450),#13277);
#12=ORIENTED_CLOSED_SHELL('',*,#6427,.F.);
#15=BREP_WITH_VOIDS('Body1',#6428,(#12));
#323=CONICAL_SURFACE('',#7373,0.325,0.785398163397448);
#324=CONICAL_SURFACE('',#7377,0.335,0.785398163397448);
#325=CONICAL_SURFACE('',#7381,0.21,0.463647609000806);
#369=SHAPE_REPRESENTATION_RELATIONSHIP('SRR','None',#13464,#406);
#406=ADVANCED_BREP_SHAPE_REPRESENTATION('',(#15),#13259);
#450=STYLED_ITEM('',(#13727),#15);
#639=FACE_BOUND('',#1667,.T.);
#808=PLANE('',#7361);
#809=PLANE('',#7362);
#810=PLANE('',#7363);
#811=PLANE('',#7364);
#812=PLANE('',#7365);
#813=PLANE('',#7366);
#814=PLANE('',#7367);
#815=PLANE('',#7368);
#816=PLANE('',#7369);
#817=PLANE('',#7371);
#818=PLANE('',#7379);
#1142=FACE_OUTER_BOUND('',#1653,.T.);
#1143=FACE_OUTER_BOUND('',#1654,.T.);
#1144=FACE_OUTER_BOUND('',#1655,.T.);
#1145=FACE_OUTER_BOUND('',#1656,.T.);
#1146=FACE_OUTER_BOUND('',#1657,.T.);
#1147=FACE_OUTER_BOUND('',#1658,.T.);
#1148=FACE_OUTER_BOUND('',#1659,.T.);
#1149=FACE_OUTER_BOUND('',#1660,.T.);
#1150=FACE_OUTER_BOUND('',#1661,.T.);
#1151=FACE_OUTER_BOUND('',#1662,.T.);
#1152=FACE_OUTER_BOUND('',#1663,.T.);
#1153=FACE_OUTER_BOUND('',#1664,.T.);
#1154=FACE_OUTER_BOUND('',#1665,.T.);
#1155=FACE_OUTER_BOUND('',#1666,.T.);
#1156=FACE_OUTER_BOUND('',#1668,.T.);
#1157=FACE_OUTER_BOUND('',#1669,.T.);
#1653=EDGE_LOOP('',(#5366,#5367,#5368,#5369));
#1654=EDGE_LOOP('',(#5370,#5371,#5372,#5373));
#1655=EDGE_LOOP('',(#5374,#5375,#5376,#5377));
#1656=EDGE_LOOP('',(#5378,#5379,#5380,#5381));
#1657=EDGE_LOOP('',(#5382,#5383,#5384,#5385));
#1658=EDGE_LOOP('',(#5386,#5387,#5388,#5389));
#1659=EDGE_LOOP('',(#5390,#5391,#5392,#5393,#5394,#5395));
#1660=EDGE_LOOP('',(#5396,#5397,#5398,#5399,#5400,#5401));
#1661=EDGE_LOOP('',(#5402));
#1662=EDGE_LOOP('',(#5403));
#1663=EDGE_LOOP('',(#5404,#5405,#5406,#5407));
#1664=EDGE_LOOP('',(#5408,#5409,#5410,#5411));
#1665=EDGE_LOOP('',(#5412,#5413,#5414,#5415));
#1666=EDGE_LOOP('',(#5416));
#1667=EDGE_LOOP('',(#5417));
#1668=EDGE_LOOP('',(#5418,#5419,#5420,#5421));
#1669=EDGE_LOOP('',(#5422,#5423,#5424,#5425));
#2098=LINE('',#12538,#2537);
#2099=LINE('',#12540,#2538);
#2100=LINE('',#12542,#2539);
#2101=LINE('',#12543,#2540);
#2102=LINE('',#12546,#2541);
#2103=LINE('',#12548,#2542);
#2104=LINE('',#12549,#2543);
#2105=LINE('',#12552,#2544);
#2106=LINE('',#12554,#2545);
#2107=LINE('',#12555,#2546);
#2108=LINE('',#12558,#2547);
#2109=LINE('',#12560,#2548);
#2110=LINE('',#12561,#2549);
#2111=LINE('',#12564,#2550);
#2112=LINE('',#12566,#2551);
#2113=LINE('',#12567,#2552);
#2114=LINE('',#12569,#2553);
#2115=LINE('',#12570,#2554);
#2116=LINE('',#12582,#2555);
#2117=LINE('',#12586,#2556);
#2118=LINE('',#12590,#2557);
#2119=LINE('',#12597,#2558);
#2120=LINE('',#12599,#2559);
#2537=VECTOR('',#8952,1.);
#2538=VECTOR('',#8953,1.);
#2539=VECTOR('',#8954,1.);
#2540=VECTOR('',#8955,1.);
#2541=VECTOR('',#8958,1.);
#2542=VECTOR('',#8959,1.);
#2543=VECTOR('',#8960,1.);
#2544=VECTOR('',#8963,1.);
#2545=VECTOR('',#8964,1.);
#2546=VECTOR('',#8965,1.);
#2547=VECTOR('',#8968,1.);
#2548=VECTOR('',#8969,1.);
#2549=VECTOR('',#8970,1.);
#2550=VECTOR('',#8973,1.);
#2551=VECTOR('',#8974,1.);
#2552=VECTOR('',#8975,1.);
#2553=VECTOR('',#8978,1.);
#2554=VECTOR('',#8979,1.);
#2555=VECTOR('',#8996,0.325);
#2556=VECTOR('',#9001,0.35);
#2557=VECTOR('',#9006,0.335);
#2558=VECTOR('',#9015,0.21);
#2559=VECTOR('',#9018,0.2);
#2946=CIRCLE('',#7370,0.1954);
#2947=CIRCLE('',#7372,0.3);
#2948=CIRCLE('',#7374,0.35);
#2949=CIRCLE('',#7376,0.35);
#2950=CIRCLE('',#7378,0.32);
#2951=CIRCLE('',#7380,0.22);
#2952=CIRCLE('',#7382,0.1954);
#3385=VERTEX_POINT('',#12536);
#3386=VERTEX_POINT('',#12537);
#3387=VERTEX_POINT('',#12539);
#3388=VERTEX_POINT('',#12541);
#3389=VERTEX_POINT('',#12545);
#3390=VERTEX_POINT('',#12547);
#3391=VERTEX_POINT('',#12551);
#3392=VERTEX_POINT('',#12553);
#3393=VERTEX_POINT('',#12557);
#3394=VERTEX_POINT('',#12559);
#3395=VERTEX_POINT('',#12563);
#3396=VERTEX_POINT('',#12565);
#3397=VERTEX_POINT('',#12574);
#3398=VERTEX_POINT('',#12577);
#3399=VERTEX_POINT('',#12580);
#3400=VERTEX_POINT('',#12584);
#3401=VERTEX_POINT('',#12588);
#3402=VERTEX_POINT('',#12592);
#3403=VERTEX_POINT('',#12595);
#4073=EDGE_CURVE('',#3385,#3386,#2098,.T.);
#4074=EDGE_CURVE('',#3386,#3387,#2099,.T.);
#4075=EDGE_CURVE('',#3387,#3388,#2100,.T.);
#4076=EDGE_CURVE('',#3385,#3388,#2101,.T.);
#4077=EDGE_CURVE('',#3386,#3389,#2102,.T.);
#4078=EDGE_CURVE('',#3389,#3390,#2103,.T.);
#4079=EDGE_CURVE('',#3390,#3387,#2104,.T.);
#4080=EDGE_CURVE('',#3389,#3391,#2105,.T.);
#4081=EDGE_CURVE('',#3391,#3392,#2106,.T.);
#4082=EDGE_CURVE('',#3392,#3390,#2107,.T.);
#4083=EDGE_CURVE('',#3391,#3393,#2108,.T.);
#4084=EDGE_CURVE('',#3393,#3394,#2109,.T.);
#4085=EDGE_CURVE('',#3394,#3392,#2110,.T.);
#4086=EDGE_CURVE('',#3393,#3395,#2111,.T.);
#4087=EDGE_CURVE('',#3395,#3396,#2112,.T.);
#4088=EDGE_CURVE('',#3396,#3394,#2113,.T.);
#4089=EDGE_CURVE('',#3395,#3385,#2114,.T.);
#4090=EDGE_CURVE('',#3388,#3396,#2115,.T.);
#4091=EDGE_CURVE('',#3397,#3397,#2946,.T.);
#4092=EDGE_CURVE('',#3398,#3398,#2947,.T.);
#4093=EDGE_CURVE('',#3399,#3399,#2948,.T.);
#4094=EDGE_CURVE('',#3399,#3398,#2116,.T.);
#4095=EDGE_CURVE('',#3400,#3400,#2949,.T.);
#4096=EDGE_CURVE('',#3400,#3399,#2117,.T.);
#4097=EDGE_CURVE('',#3401,#3401,#2950,.T.);
#4098=EDGE_CURVE('',#3401,#3400,#2118,.T.);
#4099=EDGE_CURVE('',#3402,#3402,#2951,.T.);
#4100=EDGE_CURVE('',#3403,#3403,#2952,.F.);
#4101=EDGE_CURVE('',#3403,#3402,#2119,.T.);
#4102=EDGE_CURVE('',#3397,#3403,#2120,.T.);
#5366=ORIENTED_EDGE('',*,*,#4073,.T.);
#5367=ORIENTED_EDGE('',*,*,#4074,.T.);
#5368=ORIENTED_EDGE('',*,*,#4075,.T.);
#5369=ORIENTED_EDGE('',*,*,#4076,.F.);
#5370=ORIENTED_EDGE('',*,*,#4077,.T.);
#5371=ORIENTED_EDGE('',*,*,#4078,.T.);
#5372=ORIENTED_EDGE('',*,*,#4079,.T.);
#5373=ORIENTED_EDGE('',*,*,#4074,.F.);
#5374=ORIENTED_EDGE('',*,*,#4080,.T.);
#5375=ORIENTED_EDGE('',*,*,#4081,.T.);
#5376=ORIENTED_EDGE('',*,*,#4082,.T.);
#5377=ORIENTED_EDGE('',*,*,#4078,.F.);
#5378=ORIENTED_EDGE('',*,*,#4083,.T.);
#5379=ORIENTED_EDGE('',*,*,#4084,.T.);
#5380=ORIENTED_EDGE('',*,*,#4085,.T.);
#5381=ORIENTED_EDGE('',*,*,#4081,.F.);
#5382=ORIENTED_EDGE('',*,*,#4086,.T.);
#5383=ORIENTED_EDGE('',*,*,#4087,.T.);
#5384=ORIENTED_EDGE('',*,*,#4088,.T.);
#5385=ORIENTED_EDGE('',*,*,#4084,.F.);
#5386=ORIENTED_EDGE('',*,*,#4089,.T.);
#5387=ORIENTED_EDGE('',*,*,#4076,.T.);
#5388=ORIENTED_EDGE('',*,*,#4090,.T.);
#5389=ORIENTED_EDGE('',*,*,#4087,.F.);
#5390=ORIENTED_EDGE('',*,*,#4089,.F.);
#5391=ORIENTED_EDGE('',*,*,#4086,.F.);
#5392=ORIENTED_EDGE('',*,*,#4083,.F.);
#5393=ORIENTED_EDGE('',*,*,#4080,.F.);
#5394=ORIENTED_EDGE('',*,*,#4077,.F.);
#5395=ORIENTED_EDGE('',*,*,#4073,.F.);
#5396=ORIENTED_EDGE('',*,*,#4090,.F.);
#5397=ORIENTED_EDGE('',*,*,#4075,.F.);
#5398=ORIENTED_EDGE('',*,*,#4079,.F.);
#5399=ORIENTED_EDGE('',*,*,#4082,.F.);
#5400=ORIENTED_EDGE('',*,*,#4085,.F.);
#5401=ORIENTED_EDGE('',*,*,#4088,.F.);
#5402=ORIENTED_EDGE('',*,*,#4091,.F.);
#5403=ORIENTED_EDGE('',*,*,#4092,.F.);
#5404=ORIENTED_EDGE('',*,*,#4093,.F.);
#5405=ORIENTED_EDGE('',*,*,#4094,.T.);
#5406=ORIENTED_EDGE('',*,*,#4092,.T.);
#5407=ORIENTED_EDGE('',*,*,#4094,.F.);
#5408=ORIENTED_EDGE('',*,*,#4095,.F.);
#5409=ORIENTED_EDGE('',*,*,#4096,.T.);
#5410=ORIENTED_EDGE('',*,*,#4093,.T.);
#5411=ORIENTED_EDGE('',*,*,#4096,.F.);
#5412=ORIENTED_EDGE('',*,*,#4097,.F.);
#5413=ORIENTED_EDGE('',*,*,#4098,.T.);
#5414=ORIENTED_EDGE('',*,*,#4095,.T.);
#5415=ORIENTED_EDGE('',*,*,#4098,.F.);
#5416=ORIENTED_EDGE('',*,*,#4097,.T.);
#5417=ORIENTED_EDGE('',*,*,#4099,.F.);
#5418=ORIENTED_EDGE('',*,*,#4100,.F.);
#5419=ORIENTED_EDGE('',*,*,#4101,.T.);
#5420=ORIENTED_EDGE('',*,*,#4099,.T.);
#5421=ORIENTED_EDGE('',*,*,#4101,.F.);
#5422=ORIENTED_EDGE('',*,*,#4091,.T.);
#5423=ORIENTED_EDGE('',*,*,#4102,.T.);
#5424=ORIENTED_EDGE('',*,*,#4100,.T.);
#5425=ORIENTED_EDGE('',*,*,#4102,.F.);
#5981=CYLINDRICAL_SURFACE('',#7375,0.35);
#5982=CYLINDRICAL_SURFACE('',#7383,0.1954);
#6260=ADVANCED_FACE('',(#1142),#808,.F.);
#6261=ADVANCED_FACE('',(#1143),#809,.F.);
#6262=ADVANCED_FACE('',(#1144),#810,.F.);
#6263=ADVANCED_FACE('',(#1145),#811,.F.);
#6264=ADVANCED_FACE('',(#1146),#812,.F.);
#6265=ADVANCED_FACE('',(#1147),#813,.F.);
#6266=ADVANCED_FACE('',(#1148),#814,.F.);
#6267=ADVANCED_FACE('',(#1149),#815,.F.);
#6268=ADVANCED_FACE('',(#1150),#816,.F.);
#6269=ADVANCED_FACE('',(#1151),#817,.T.);
#6270=ADVANCED_FACE('',(#1152),#323,.T.);
#6271=ADVANCED_FACE('',(#1153),#5981,.T.);
#6272=ADVANCED_FACE('',(#1154),#324,.T.);
#6273=ADVANCED_FACE('',(#1155,#639),#818,.T.);
#6274=ADVANCED_FACE('',(#1156),#325,.T.);
#6275=ADVANCED_FACE('',(#1157),#5982,.T.);
#6427=CLOSED_SHELL('',(#6260,#6261,#6262,#6263,#6264,#6265,#6266,#6267));
#6428=CLOSED_SHELL('',(#6268,#6269,#6270,#6271,#6272,#6273,#6274,#6275));
#7360=AXIS2_PLACEMENT_3D('',#12534,#8948,#8949);
#7361=AXIS2_PLACEMENT_3D('',#12535,#8950,#8951);
#7362=AXIS2_PLACEMENT_3D('',#12544,#8956,#8957);
#7363=AXIS2_PLACEMENT_3D('',#12550,#8961,#8962);
#7364=AXIS2_PLACEMENT_3D('',#12556,#8966,#8967);
#7365=AXIS2_PLACEMENT_3D('',#12562,#8971,#8972);
#7366=AXIS2_PLACEMENT_3D('',#12568,#8976,#8977);
#7367=AXIS2_PLACEMENT_3D('',#12571,#8980,#8981);
#7368=AXIS2_PLACEMENT_3D('',#12572,#8982,#8983);
#7369=AXIS2_PLACEMENT_3D('',#12573,#8984,#8985);
#7370=AXIS2_PLACEMENT_3D('',#12575,#8986,#8987);
#7371=AXIS2_PLACEMENT_3D('',#12576,#8988,#8989);
#7372=AXIS2_PLACEMENT_3D('',#12578,#8990,#8991);
#7373=AXIS2_PLACEMENT_3D('',#12579,#8992,#8993);
#7374=AXIS2_PLACEMENT_3D('',#12581,#8994,#8995);
#7375=AXIS2_PLACEMENT_3D('',#12583,#8997,#8998);
#7376=AXIS2_PLACEMENT_3D('',#12585,#8999,#9000);
#7377=AXIS2_PLACEMENT_3D('',#12587,#9002,#9003);
#7378=AXIS2_PLACEMENT_3D('',#12589,#9004,#9005);
#7379=AXIS2_PLACEMENT_3D('',#12591,#9007,#9008);
#7380=AXIS2_PLACEMENT_3D('',#12593,#9009,#9010);
#7381=AXIS2_PLACEMENT_3D('',#12594,#9011,#9012);
#7382=AXIS2_PLACEMENT_3D('',#12596,#9013,#9014);
#7383=AXIS2_PLACEMENT_3D('',#12598,#9016,#9017);
#8948=DIRECTION('axis',(0.,0.,1.));
#8949=DIRECTION('refdir',(1.,0.,0.));
#8950=DIRECTION('center_axis',(0.866025403784439,0.,-0.5));
#8951=DIRECTION('ref_axis',(0.5,0.,0.866025403784439));
#8952=DIRECTION('',(-0.5,0.,-0.866025403784439));
#8953=DIRECTION('',(0.,-1.,0.));
#8954=DIRECTION('',(0.5,0.,0.866025403784439));
#8955=DIRECTION('',(0.,-1.,0.));
#8956=DIRECTION('center_axis',(1.60246890531964E-16,0.,-1.));
#8957=DIRECTION('ref_axis',(1.,0.,1.60246890531964E-16));
#8958=DIRECTION('',(-1.,0.,-1.60246890531964E-16));
#8959=DIRECTION('',(0.,-1.,0.));
#8960=DIRECTION('',(1.,0.,1.60246890531964E-16));
#8961=DIRECTION('center_axis',(-0.866025403784439,0.,-0.5));
#8962=DIRECTION('ref_axis',(0.5,0.,-0.866025403784439));
#8963=DIRECTION('',(-0.5,0.,0.866025403784439));
#8964=DIRECTION('',(0.,-1.,0.));
#8965=DIRECTION('',(0.5,0.,-0.866025403784439));
#8966=DIRECTION('center_axis',(-0.866025403784439,0.,0.5));
#8967=DIRECTION('ref_axis',(-0.5,0.,-0.866025403784439));
#8968=DIRECTION('',(0.5,0.,0.866025403784439));
#8969=DIRECTION('',(0.,-1.,0.));
#8970=DIRECTION('',(-0.5,0.,-0.866025403784439));
#8971=DIRECTION('center_axis',(-1.60246890531964E-16,0.,1.));
#8972=DIRECTION('ref_axis',(-1.,0.,-1.60246890531964E-16));
#8973=DIRECTION('',(1.,0.,1.60246890531964E-16));
#8974=DIRECTION('',(0.,-1.,0.));
#8975=DIRECTION('',(-1.,0.,-1.60246890531964E-16));
#8976=DIRECTION('center_axis',(0.866025403784439,0.,0.5));
#8977=DIRECTION('ref_axis',(-0.5,0.,0.866025403784439));
#8978=DIRECTION('',(0.5,0.,-0.866025403784439));
#8979=DIRECTION('',(-0.5,0.,0.866025403784439));
#8980=DIRECTION('center_axis',(0.,1.,0.));
#8981=DIRECTION('ref_axis',(1.,0.,0.));
#8982=DIRECTION('center_axis',(0.,-1.,0.));
#8983=DIRECTION('ref_axis',(0.,0.,-1.));
#8984=DIRECTION('center_axis',(0.,1.,0.));
#8985=DIRECTION('ref_axis',(1.,0.,0.));
#8986=DIRECTION('center_axis',(0.,1.,0.));
#8987=DIRECTION('ref_axis',(1.,0.,0.));
#8988=DIRECTION('center_axis',(0.,1.,0.));
#8989=DIRECTION('ref_axis',(0.,0.,1.));
#8990=DIRECTION('center_axis',(0.,-1.,0.));
#8991=DIRECTION('ref_axis',(1.,0.,0.));
#8992=DIRECTION('center_axis',(0.,-1.,0.));
#8993=DIRECTION('ref_axis',(1.,0.,0.));
#8994=DIRECTION('center_axis',(0.,-1.,0.));
#8995=DIRECTION('ref_axis',(1.,0.,0.));
#8996=DIRECTION('',(0.707106781186547,0.707106781186548,8.65956056235493E-17));
#8997=DIRECTION('center_axis',(0.,-1.,0.));
#8998=DIRECTION('ref_axis',(1.,0.,0.));
#8999=DIRECTION('center_axis',(0.,-1.,0.));
#9000=DIRECTION('ref_axis',(1.,0.,0.));
#9001=DIRECTION('',(0.,1.,0.));
#9002=DIRECTION('center_axis',(0.,1.,0.));
#9003=DIRECTION('ref_axis',(1.,0.,0.));
#9004=DIRECTION('center_axis',(0.,-1.,0.));
#9005=DIRECTION('ref_axis',(1.,0.,0.));
#9006=DIRECTION('',(-0.707106781186547,0.707106781186548,-8.65956056235493E-17));
#9007=DIRECTION('center_axis',(0.,-1.,0.));
#9008=DIRECTION('ref_axis',(0.,0.,-1.));
#9009=DIRECTION('center_axis',(0.,-1.,0.));
#9010=DIRECTION('ref_axis',(1.,0.,0.));
#9011=DIRECTION('center_axis',(0.,1.,0.));
#9012=DIRECTION('ref_axis',(1.,0.,0.));
#9013=DIRECTION('center_axis',(0.,1.,0.));
#9014=DIRECTION('ref_axis',(1.,0.,0.));
#9015=DIRECTION('',(-0.447213595499958,0.894427190999916,-5.47678698264203E-17));
#9016=DIRECTION('center_axis',(0.,-1.,0.));
#9017=DIRECTION('ref_axis',(1.,0.,0.));
#9018=DIRECTION('',(0.,1.,0.));
#12534=CARTESIAN_POINT('',(0.,0.,0.));
#12535=CARTESIAN_POINT('Origin',(0.0866025403784439,-0.4,-0.15));
#12536=CARTESIAN_POINT('',(0.173205080756888,-0.4,0.));
#12537=CARTESIAN_POINT('',(0.0866025403784439,-0.4,-0.15));
#12538=CARTESIAN_POINT('',(0.173205080756888,-0.4,0.));
#12539=CARTESIAN_POINT('',(0.0866025403784439,-0.64,-0.15));
#12540=CARTESIAN_POINT('',(0.0866025403784439,-0.4,-0.15));
#12541=CARTESIAN_POINT('',(0.173205080756888,-0.64,0.));
#12542=CARTESIAN_POINT('',(0.173205080756888,-0.64,0.));
#12543=CARTESIAN_POINT('',(0.173205080756888,-0.4,0.));
#12544=CARTESIAN_POINT('Origin',(-0.0866025403784438,-0.4,-0.15));
#12545=CARTESIAN_POINT('',(-0.0866025403784438,-0.4,-0.15));
#12546=CARTESIAN_POINT('',(0.0866025403784439,-0.4,-0.15));
#12547=CARTESIAN_POINT('',(-0.0866025403784438,-0.64,-0.15));
#12548=CARTESIAN_POINT('',(-0.0866025403784438,-0.4,-0.15));
#12549=CARTESIAN_POINT('',(0.0866025403784439,-0.64,-0.15));
#12550=CARTESIAN_POINT('Origin',(-0.173205080756888,-0.4,-2.77555756156289E-17));
#12551=CARTESIAN_POINT('',(-0.173205080756888,-0.4,-2.12115047744981E-17));
#12552=CARTESIAN_POINT('',(-0.0866025403784438,-0.4,-0.15));
#12553=CARTESIAN_POINT('',(-0.173205080756888,-0.64,-2.77555756156289E-17));
#12554=CARTESIAN_POINT('',(-0.173205080756888,-0.4,-2.12115047744981E-17));
#12555=CARTESIAN_POINT('',(-0.0866025403784438,-0.64,-0.15));
#12556=CARTESIAN_POINT('Origin',(-0.0866025403784439,-0.4,0.15));
#12557=CARTESIAN_POINT('',(-0.0866025403784439,-0.4,0.15));
#12558=CARTESIAN_POINT('',(-0.173205080756888,-0.4,-2.12115047744981E-17));
#12559=CARTESIAN_POINT('',(-0.0866025403784439,-0.64,0.15));
#12560=CARTESIAN_POINT('',(-0.0866025403784439,-0.4,0.15));
#12561=CARTESIAN_POINT('',(-0.173205080756888,-0.64,-2.12115047744981E-17));
#12562=CARTESIAN_POINT('Origin',(0.0866025403784439,-0.4,0.15));
#12563=CARTESIAN_POINT('',(0.0866025403784439,-0.4,0.15));
#12564=CARTESIAN_POINT('',(-0.0866025403784439,-0.4,0.15));
#12565=CARTESIAN_POINT('',(0.0866025403784439,-0.64,0.15));
#12566=CARTESIAN_POINT('',(0.0866025403784439,-0.4,0.15));
#12567=CARTESIAN_POINT('',(-0.0866025403784439,-0.64,0.15));
#12568=CARTESIAN_POINT('Origin',(0.173205080756888,-0.4,0.));
#12569=CARTESIAN_POINT('',(0.0866025403784439,-0.4,0.15));
#12570=CARTESIAN_POINT('',(0.0866025403784439,-0.64,0.15));
#12571=CARTESIAN_POINT('Origin',(0.,-0.4,-2.77555756156289E-17));
#12572=CARTESIAN_POINT('Origin',(0.,-0.64,-2.77555756156289E-17));
#12573=CARTESIAN_POINT('Origin',(0.,-1.,0.));
#12574=CARTESIAN_POINT('',(-0.1954,-1.,2.39295984553393E-17));
#12575=CARTESIAN_POINT('Origin',(0.,-1.,0.));
#12576=CARTESIAN_POINT('Origin',(0.3,0.4,0.));
#12577=CARTESIAN_POINT('',(-0.3,0.4,-3.67394039744206E-17));
#12578=CARTESIAN_POINT('Origin',(0.,0.4,0.));
#12579=CARTESIAN_POINT('Origin',(0.,0.375,0.));
#12580=CARTESIAN_POINT('',(-0.35,0.35,-4.28626379701573E-17));
#12581=CARTESIAN_POINT('Origin',(0.,0.35,0.));
#12582=CARTESIAN_POINT('',(-0.325,0.375,-3.9801020972289E-17));
#12583=CARTESIAN_POINT('Origin',(0.,0.19,0.));
#12584=CARTESIAN_POINT('',(-0.35,0.03,-4.28626379701574E-17));
#12585=CARTESIAN_POINT('Origin',(0.,0.03,0.));
#12586=CARTESIAN_POINT('',(-0.35,0.19,-4.28626379701574E-17));
#12587=CARTESIAN_POINT('Origin',(0.,0.0149999999999999,0.));
#12588=CARTESIAN_POINT('',(-0.32,-3.29597460435593E-17,-3.91886975727153E-17));
#12589=CARTESIAN_POINT('Origin',(0.,0.,0.));
#12590=CARTESIAN_POINT('',(-0.335,0.0149999999999999,-4.10256677714363E-17));
#12591=CARTESIAN_POINT('Origin',(0.22,0.,0.));
#12592=CARTESIAN_POINT('',(-0.22,-6.93889390390723E-18,-2.69422295812418E-17));
#12593=CARTESIAN_POINT('Origin',(0.,0.,0.));
#12594=CARTESIAN_POINT('Origin',(0.,-0.02,0.));
#12595=CARTESIAN_POINT('',(-0.1954,-0.0492,2.39295984553393E-17));
#12596=CARTESIAN_POINT('Origin',(0.,-0.0492,0.));
#12597=CARTESIAN_POINT('',(-0.21,-0.02,-2.57175827820944E-17));
#12598=CARTESIAN_POINT('Origin',(0.,-0.8,0.));
#12599=CARTESIAN_POINT('',(-0.1954,-0.8,-2.39295984553393E-17));
#13215=UNCERTAINTY_MEASURE_WITH_UNIT(LENGTH_MEASURE(0.001),#13278,
'DISTANCE_ACCURACY_VALUE',
'Maximum model space distance between geometric entities at asserted c
onnectivities');
#13233=UNCERTAINTY_MEASURE_WITH_UNIT(LENGTH_MEASURE(0.001),#13278,
'DISTANCE_ACCURACY_VALUE',
'Maximum model space distance between geometric entities at asserted c
onnectivities');
#13259=(
GEOMETRIC_REPRESENTATION_CONTEXT(3)
GLOBAL_UNCERTAINTY_ASSIGNED_CONTEXT((#13215))
GLOBAL_UNIT_ASSIGNED_CONTEXT((#13278,#13280,#13281))
REPRESENTATION_CONTEXT('','3D')
);
#13277=(
GEOMETRIC_REPRESENTATION_CONTEXT(3)
GLOBAL_UNCERTAINTY_ASSIGNED_CONTEXT((#13233))
GLOBAL_UNIT_ASSIGNED_CONTEXT((#13278,#13280,#13281))
REPRESENTATION_CONTEXT('','3D')
);
#13278=(
LENGTH_UNIT()
NAMED_UNIT(*)
SI_UNIT(.CENTI.,.METRE.)
);
#13280=(
NAMED_UNIT(*)
PLANE_ANGLE_UNIT()
SI_UNIT($,.RADIAN.)
);
#13281=(
NAMED_UNIT(*)
SI_UNIT($,.STERADIAN.)
SOLID_ANGLE_UNIT()
);
#13307=SHAPE_DEFINITION_REPRESENTATION(#13357,#13464);
#13357=PRODUCT_DEFINITION_SHAPE('',$,#13508);
#13464=SHAPE_REPRESENTATION('',(#7360),#13259);
#13482=PRODUCT_DEFINITION_CONTEXT('part definition',#13613,'design');
#13508=PRODUCT_DEFINITION('M4x10 Cap Screw','M4x10 Cap Screw',#13551,#13482);
#13551=PRODUCT_DEFINITION_FORMATION('',$,#13640);
#13613=APPLICATION_CONTEXT(
'Core Data for Automotive Mechanical Design Process');
#13614=PRODUCT_CONTEXT('part definition',#13613,'mechanical');
#13640=PRODUCT('M4x10 Cap Screw','M4x10 Cap Screw','M4x10 Cap Screw',(#13614));
#13721=COLOUR_RGB('Black',0.12,0.14,0.17);
#13722=FILL_AREA_STYLE_COLOUR('',#13721);
#13723=FILL_AREA_STYLE('',(#13722));
#13724=SURFACE_STYLE_FILL_AREA(#13723);
#13725=SURFACE_SIDE_STYLE('',(#13724));
#13726=SURFACE_STYLE_USAGE(.BOTH.,#13725);
#13727=PRESENTATION_STYLE_ASSIGNMENT((#13726));
ENDSEC;
END-ISO-10303-21;
